ISO-10303-21;
HEADER;
/* Generated by software containing ST-Developer
 * from STEP Tools, Inc. (www.steptools.com) 
 */

FILE_DESCRIPTION(
/* description */ ('Cam-driven reciprocating slide'),
/* implementation_level */ '2;1');

FILE_NAME(
/* name */ 'Bearing cap (1).step',
/* time_stamp */ '2026-10-28T03:25:20-07:00',
/* author */ (''),
/* organization */ (''),
/* preprocessor_version */ 'ST-DEVELOPER v20.2',
/* originating_system */ 'Autodesk Translation Framework v15.17.0.0',
/* authorisation */ '');

FILE_SCHEMA (('AUTOMOTIVE_DESIGN { 1 0 10303 214 3 1 1 }'));
ENDSEC;

DATA;
#10=MECHANICAL_DESIGN_GEOMETRIC_PRESENTATION_REPRESENTATION('',(#427),#13277);
#353=SHAPE_REPRESENTATION_RELATIONSHIP('SRR','None',#13446,#390);
#390=ADVANCED_BREP_SHAPE_REPRESENTATION('',(#471),#13241);
#427=STYLED_ITEM('',(#13720),#471);
#471=MANIFOLD_SOLID_BREP('Body1',#6403);
#545=FACE_BOUND('',#1380,.T.);
#546=FACE_BOUND('',#1384,.T.);
#547=FACE_BOUND('',#1385,.T.);
#548=FACE_BOUND('',#1386,.T.);
#549=FACE_BOUND('',#1387,.T.);
#550=FACE_BOUND('',#1388,.T.);
#551=FACE_BOUND('',#1390,.T.);
#552=FACE_BOUND('',#1391,.T.);
#553=FACE_BOUND('',#1392,.T.);
#554=FACE_BOUND('',#1393,.T.);
#555=FACE_BOUND('',#1394,.T.);
#717=PLANE('',#6972);
#718=PLANE('',#6979);
#719=PLANE('',#6980);
#957=FACE_OUTER_BOUND('',#1374,.T.);
#958=FACE_OUTER_BOUND('',#1375,.T.);
#959=FACE_OUTER_BOUND('',#1376,.T.);
#960=FACE_OUTER_BOUND('',#1377,.T.);
#961=FACE_OUTER_BOUND('',#1378,.T.);
#962=FACE_OUTER_BOUND('',#1379,.T.);
#963=FACE_OUTER_BOUND('',#1381,.T.);
#964=FACE_OUTER_BOUND('',#1382,.T.);
#965=FACE_OUTER_BOUND('',#1383,.T.);
#966=FACE_OUTER_BOUND('',#1389,.T.);
#1374=EDGE_LOOP('',(#4600,#4601,#4602,#4603));
#1375=EDGE_LOOP('',(#4604,#4605,#4606,#4607));
#1376=EDGE_LOOP('',(#4608,#4609,#4610,#4611));
#1377=EDGE_LOOP('',(#4612,#4613,#4614,#4615));
#1378=EDGE_LOOP('',(#4616,#4617,#4618,#4619));
#1379=EDGE_LOOP('',(#4620));
#1380=EDGE_LOOP('',(#4621));
#1381=EDGE_LOOP('',(#4622,#4623,#4624,#4625));
#1382=EDGE_LOOP('',(#4626,#4627,#4628,#4629));
#1383=EDGE_LOOP('',(#4630));
#1384=EDGE_LOOP('',(#4631));
#1385=EDGE_LOOP('',(#4632));
#1386=EDGE_LOOP('',(#4633));
#1387=EDGE_LOOP('',(#4634));
#1388=EDGE_LOOP('',(#4635));
#1389=EDGE_LOOP('',(#4636));
#1390=EDGE_LOOP('',(#4637));
#1391=EDGE_LOOP('',(#4638));
#1392=EDGE_LOOP('',(#4639));
#1393=EDGE_LOOP('',(#4640));
#1394=EDGE_LOOP('',(#4641));
#1925=LINE('',#10028,#2364);
#1926=LINE('',#10034,#2365);
#1927=LINE('',#10040,#2366);
#1928=LINE('',#10046,#2367);
#1929=LINE('',#10052,#2368);
#1930=LINE('',#10060,#2369);
#1931=LINE('',#10065,#2370);
#2364=VECTOR('',#7973,0.225);
#2365=VECTOR('',#7980,0.225);
#2366=VECTOR('',#7987,0.225);
#2367=VECTOR('',#7994,0.225);
#2368=VECTOR('',#8001,1.59);
#2369=VECTOR('',#8012,1.005);
#2370=VECTOR('',#8017,2.4);
#2751=CIRCLE('',#6958,0.225);
#2752=CIRCLE('',#6959,0.225);
#2753=CIRCLE('',#6961,0.225);
#2754=CIRCLE('',#6962,0.225);
#2755=CIRCLE('',#6964,0.225);
#2756=CIRCLE('',#6965,0.225);
#2757=CIRCLE('',#6967,0.225);
#2758=CIRCLE('',#6968,0.225);
#2759=CIRCLE('',#6970,1.59);
#2760=CIRCLE('',#6971,1.59);
#2761=CIRCLE('',#6973,1.005);
#2762=CIRCLE('',#6975,1.005);
#2763=CIRCLE('',#6977,2.4);
#2764=CIRCLE('',#6978,2.4);
#3123=VERTEX_POINT('',#10025);
#3124=VERTEX_POINT('',#10027);
#3125=VERTEX_POINT('',#10031);
#3126=VERTEX_POINT('',#10033);
#3127=VERTEX_POINT('',#10037);
#3128=VERTEX_POINT('',#10039);
#3129=VERTEX_POINT('',#10043);
#3130=VERTEX_POINT('',#10045);
#3131=VERTEX_POINT('',#10049);
#3132=VERTEX_POINT('',#10051);
#3133=VERTEX_POINT('',#10055);
#3134=VERTEX_POINT('',#10058);
#3135=VERTEX_POINT('',#10062);
#3136=VERTEX_POINT('',#10064);
#3690=EDGE_CURVE('',#3123,#3123,#2751,.T.);
#3691=EDGE_CURVE('',#3123,#3124,#1925,.T.);
#3692=EDGE_CURVE('',#3124,#3124,#2752,.T.);
#3693=EDGE_CURVE('',#3125,#3125,#2753,.T.);
#3694=EDGE_CURVE('',#3125,#3126,#1926,.T.);
#3695=EDGE_CURVE('',#3126,#3126,#2754,.T.);
#3696=EDGE_CURVE('',#3127,#3127,#2755,.T.);
#3697=EDGE_CURVE('',#3127,#3128,#1927,.T.);
#3698=EDGE_CURVE('',#3128,#3128,#2756,.T.);
#3699=EDGE_CURVE('',#3129,#3129,#2757,.T.);
#3700=EDGE_CURVE('',#3129,#3130,#1928,.T.);
#3701=EDGE_CURVE('',#3130,#3130,#2758,.T.);
#3702=EDGE_CURVE('',#3131,#3131,#2759,.T.);
#3703=EDGE_CURVE('',#3131,#3132,#1929,.T.);
#3704=EDGE_CURVE('',#3132,#3132,#2760,.T.);
#3705=EDGE_CURVE('',#3133,#3133,#2761,.T.);
#3706=EDGE_CURVE('',#3134,#3134,#2762,.T.);
#3707=EDGE_CURVE('',#3134,#3133,#1930,.T.);
#3708=EDGE_CURVE('',#3135,#3135,#2763,.T.);
#3709=EDGE_CURVE('',#3135,#3136,#1931,.T.);
#3710=EDGE_CURVE('',#3136,#3136,#2764,.T.);
#4600=ORIENTED_EDGE('',*,*,#3690,.F.);
#4601=ORIENTED_EDGE('',*,*,#3691,.T.);
#4602=ORIENTED_EDGE('',*,*,#3692,.F.);
#4603=ORIENTED_EDGE('',*,*,#3691,.F.);
#4604=ORIENTED_EDGE('',*,*,#3693,.F.);
#4605=ORIENTED_EDGE('',*,*,#3694,.T.);
#4606=ORIENTED_EDGE('',*,*,#3695,.F.);
#4607=ORIENTED_EDGE('',*,*,#3694,.F.);
#4608=ORIENTED_EDGE('',*,*,#3696,.F.);
#4609=ORIENTED_EDGE('',*,*,#3697,.T.);
#4610=ORIENTED_EDGE('',*,*,#3698,.F.);
#4611=ORIENTED_EDGE('',*,*,#3697,.F.);
#4612=ORIENTED_EDGE('',*,*,#3699,.F.);
#4613=ORIENTED_EDGE('',*,*,#3700,.T.);
#4614=ORIENTED_EDGE('',*,*,#3701,.F.);
#4615=ORIENTED_EDGE('',*,*,#3700,.F.);
#4616=ORIENTED_EDGE('',*,*,#3702,.F.);
#4617=ORIENTED_EDGE('',*,*,#3703,.T.);
#4618=ORIENTED_EDGE('',*,*,#3704,.T.);
#4619=ORIENTED_EDGE('',*,*,#3703,.F.);
#4620=ORIENTED_EDGE('',*,*,#3704,.F.);
#4621=ORIENTED_EDGE('',*,*,#3705,.F.);
#4622=ORIENTED_EDGE('',*,*,#3706,.F.);
#4623=ORIENTED_EDGE('',*,*,#3707,.T.);
#4624=ORIENTED_EDGE('',*,*,#3705,.T.);
#4625=ORIENTED_EDGE('',*,*,#3707,.F.);
#4626=ORIENTED_EDGE('',*,*,#3708,.F.);
#4627=ORIENTED_EDGE('',*,*,#3709,.T.);
#4628=ORIENTED_EDGE('',*,*,#3710,.T.);
#4629=ORIENTED_EDGE('',*,*,#3709,.F.);
#4630=ORIENTED_EDGE('',*,*,#3708,.T.);
#4631=ORIENTED_EDGE('',*,*,#3706,.T.);
#4632=ORIENTED_EDGE('',*,*,#3701,.T.);
#4633=ORIENTED_EDGE('',*,*,#3698,.T.);
#4634=ORIENTED_EDGE('',*,*,#3695,.T.);
#4635=ORIENTED_EDGE('',*,*,#3692,.T.);
#4636=ORIENTED_EDGE('',*,*,#3710,.F.);
#4637=ORIENTED_EDGE('',*,*,#3702,.T.);
#4638=ORIENTED_EDGE('',*,*,#3699,.T.);
#4639=ORIENTED_EDGE('',*,*,#3696,.T.);
#4640=ORIENTED_EDGE('',*,*,#3693,.T.);
#4641=ORIENTED_EDGE('',*,*,#3690,.T.);
#5912=CYLINDRICAL_SURFACE('',#6957,0.225);
#5913=CYLINDRICAL_SURFACE('',#6960,0.225);
#5914=CYLINDRICAL_SURFACE('',#6963,0.225);
#5915=CYLINDRICAL_SURFACE('',#6966,0.225);
#5916=CYLINDRICAL_SURFACE('',#6969,1.59);
#5917=CYLINDRICAL_SURFACE('',#6974,1.005);
#5918=CYLINDRICAL_SURFACE('',#6976,2.4);
#6075=ADVANCED_FACE('',(#957),#5912,.F.);
#6076=ADVANCED_FACE('',(#958),#5913,.F.);
#6077=ADVANCED_FACE('',(#959),#5914,.F.);
#6078=ADVANCED_FACE('',(#960),#5915,.F.);
#6079=ADVANCED_FACE('',(#961),#5916,.T.);
#6080=ADVANCED_FACE('',(#962,#545),#717,.F.);
#6081=ADVANCED_FACE('',(#963),#5917,.F.);
#6082=ADVANCED_FACE('',(#964),#5918,.T.);
#6083=ADVANCED_FACE('',(#965,#546,#547,#548,#549,#550),#718,.T.);
#6084=ADVANCED_FACE('',(#966,#551,#552,#553,#554,#555),#719,.F.);
#6403=CLOSED_SHELL('',(#6075,#6076,#6077,#6078,#6079,#6080,#6081,#6082,
#6083,#6084));
#6956=AXIS2_PLACEMENT_3D('',#10023,#7967,#7968);
#6957=AXIS2_PLACEMENT_3D('',#10024,#7969,#7970);
#6958=AXIS2_PLACEMENT_3D('',#10026,#7971,#7972);
#6959=AXIS2_PLACEMENT_3D('',#10029,#7974,#7975);
#6960=AXIS2_PLACEMENT_3D('',#10030,#7976,#7977);
#6961=AXIS2_PLACEMENT_3D('',#10032,#7978,#7979);
#6962=AXIS2_PLACEMENT_3D('',#10035,#7981,#7982);
#6963=AXIS2_PLACEMENT_3D('',#10036,#7983,#7984);
#6964=AXIS2_PLACEMENT_3D('',#10038,#7985,#7986);
#6965=AXIS2_PLACEMENT_3D('',#10041,#7988,#7989);
#6966=AXIS2_PLACEMENT_3D('',#10042,#7990,#7991);
#6967=AXIS2_PLACEMENT_3D('',#10044,#7992,#7993);
#6968=AXIS2_PLACEMENT_3D('',#10047,#7995,#7996);
#6969=AXIS2_PLACEMENT_3D('',#10048,#7997,#7998);
#6970=AXIS2_PLACEMENT_3D('',#10050,#7999,#8000);
#6971=AXIS2_PLACEMENT_3D('',#10053,#8002,#8003);
#6972=AXIS2_PLACEMENT_3D('',#10054,#8004,#8005);
#6973=AXIS2_PLACEMENT_3D('',#10056,#8006,#8007);
#6974=AXIS2_PLACEMENT_3D('',#10057,#8008,#8009);
#6975=AXIS2_PLACEMENT_3D('',#10059,#8010,#8011);
#6976=AXIS2_PLACEMENT_3D('',#10061,#8013,#8014);
#6977=AXIS2_PLACEMENT_3D('',#10063,#8015,#8016);
#6978=AXIS2_PLACEMENT_3D('',#10066,#8018,#8019);
#6979=AXIS2_PLACEMENT_3D('',#10067,#8020,#8021);
#6980=AXIS2_PLACEMENT_3D('',#10068,#8022,#8023);
#7967=DIRECTION('axis',(0.,0.,1.));
#7968=DIRECTION('refdir',(1.,0.,0.));
#7969=DIRECTION('center_axis',(0.,1.,0.));
#7970=DIRECTION('ref_axis',(1.,0.,0.));
#7971=DIRECTION('center_axis',(0.,1.,0.));
#7972=DIRECTION('ref_axis',(1.,0.,0.));
#7973=DIRECTION('',(0.,1.,0.));
#7974=DIRECTION('center_axis',(0.,-1.,0.));
#7975=DIRECTION('ref_axis',(1.,0.,0.));
#7976=DIRECTION('center_axis',(0.,1.,0.));
#7977=DIRECTION('ref_axis',(1.,0.,0.));
#7978=DIRECTION('center_axis',(0.,1.,0.));
#7979=DIRECTION('ref_axis',(1.,0.,0.));
#7980=DIRECTION('',(0.,1.,0.));
#7981=DIRECTION('center_axis',(0.,-1.,0.));
#7982=DIRECTION('ref_axis',(1.,0.,0.));
#7983=DIRECTION('center_axis',(0.,1.,0.));
#7984=DIRECTION('ref_axis',(1.,0.,0.));
#7985=DIRECTION('center_axis',(0.,1.,0.));
#7986=DIRECTION('ref_axis',(1.,0.,0.));
#7987=DIRECTION('',(0.,1.,0.));
#7988=DIRECTION('center_axis',(0.,-1.,0.));
#7989=DIRECTION('ref_axis',(1.,0.,0.));
#7990=DIRECTION('center_axis',(0.,1.,0.));
#7991=DIRECTION('ref_axis',(1.,0.,0.));
#7992=DIRECTION('center_axis',(0.,1.,0.));
#7993=DIRECTION('ref_axis',(1.,0.,0.));
#7994=DIRECTION('',(0.,1.,0.));
#7995=DIRECTION('center_axis',(0.,-1.,0.));
#7996=DIRECTION('ref_axis',(1.,0.,0.));
#7997=DIRECTION('center_axis',(0.,1.,0.));
#7998=DIRECTION('ref_axis',(1.,0.,0.));
#7999=DIRECTION('center_axis',(0.,1.,0.));
#8000=DIRECTION('ref_axis',(1.,0.,0.));
#8001=DIRECTION('',(0.,-1.,0.));
#8002=DIRECTION('center_axis',(0.,1.,0.));
#8003=DIRECTION('ref_axis',(1.,0.,0.));
#8004=DIRECTION('center_axis',(0.,1.,0.));
#8005=DIRECTION('ref_axis',(1.,0.,0.));
#8006=DIRECTION('center_axis',(0.,-1.,0.));
#8007=DIRECTION('ref_axis',(1.,0.,0.));
#8008=DIRECTION('center_axis',(0.,1.,0.));
#8009=DIRECTION('ref_axis',(1.,0.,0.));
#8010=DIRECTION('center_axis',(0.,-1.,0.));
#8011=DIRECTION('ref_axis',(1.,0.,0.));
#8012=DIRECTION('',(0.,-1.,0.));
#8013=DIRECTION('center_axis',(0.,1.,0.));
#8014=DIRECTION('ref_axis',(1.,0.,0.));
#8015=DIRECTION('center_axis',(0.,1.,0.));
#8016=DIRECTION('ref_axis',(1.,0.,0.));
#8017=DIRECTION('',(0.,-1.,0.));
#8018=DIRECTION('center_axis',(0.,1.,0.));
#8019=DIRECTION('ref_axis',(1.,0.,0.));
#8020=DIRECTION('center_axis',(0.,1.,0.));
#8021=DIRECTION('ref_axis',(1.,0.,0.));
#8022=DIRECTION('center_axis',(0.,1.,0.));
#8023=DIRECTION('ref_axis',(1.,0.,0.));
#10023=CARTESIAN_POINT('',(0.,0.,0.));
#10024=CARTESIAN_POINT('Origin',(-1.4142135623731,-1.8,2.58578643762691));
#10025=CARTESIAN_POINT('',(-1.6392135623731,-1.7,2.58578643762691));
#10026=CARTESIAN_POINT('Origin',(-1.4142135623731,-1.7,2.58578643762691));
#10027=CARTESIAN_POINT('',(-1.6392135623731,-1.5,2.58578643762691));
#10028=CARTESIAN_POINT('',(-1.6392135623731,-1.8,2.58578643762691));
#10029=CARTESIAN_POINT('Origin',(-1.4142135623731,-1.5,2.58578643762691));
#10030=CARTESIAN_POINT('Origin',(-1.41421356237309,-1.8,5.41421356237309));
#10031=CARTESIAN_POINT('',(-1.6392135623731,-1.7,5.41421356237309));
#10032=CARTESIAN_POINT('Origin',(-1.41421356237309,-1.7,5.41421356237309));
#10033=CARTESIAN_POINT('',(-1.6392135623731,-1.5,5.41421356237309));
#10034=CARTESIAN_POINT('',(-1.6392135623731,-1.8,5.41421356237309));
#10035=CARTESIAN_POINT('Origin',(-1.41421356237309,-1.5,5.41421356237309));
#10036=CARTESIAN_POINT('Origin',(1.4142135623731,-1.8,5.41421356237309));
#10037=CARTESIAN_POINT('',(1.1892135623731,-1.7,5.41421356237309));
#10038=CARTESIAN_POINT('Origin',(1.4142135623731,-1.7,5.41421356237309));
#10039=CARTESIAN_POINT('',(1.1892135623731,-1.5,5.41421356237309));
#10040=CARTESIAN_POINT('',(1.1892135623731,-1.8,5.41421356237309));
#10041=CARTESIAN_POINT('Origin',(1.4142135623731,-1.5,5.41421356237309));
#10042=CARTESIAN_POINT('Origin',(1.41421356237309,-1.8,2.5857864376269));
#10043=CARTESIAN_POINT('',(1.18921356237309,-1.7,2.5857864376269));
#10044=CARTESIAN_POINT('Origin',(1.41421356237309,-1.7,2.5857864376269));
#10045=CARTESIAN_POINT('',(1.18921356237309,-1.5,2.5857864376269));
#10046=CARTESIAN_POINT('',(1.18921356237309,-1.8,2.5857864376269));
#10047=CARTESIAN_POINT('Origin',(1.41421356237309,-1.5,2.5857864376269));
#10048=CARTESIAN_POINT('Origin',(0.,-2.,4.));
#10049=CARTESIAN_POINT('',(-1.59,-1.7,4.));
#10050=CARTESIAN_POINT('Origin',(0.,-1.7,4.));
#10051=CARTESIAN_POINT('',(-1.59,-2.,4.));
#10052=CARTESIAN_POINT('',(-1.59,-2.,4.));
#10053=CARTESIAN_POINT('Origin',(0.,-2.,4.));
#10054=CARTESIAN_POINT('Origin',(0.,-2.,4.));
#10055=CARTESIAN_POINT('',(-1.005,-2.,4.));
#10056=CARTESIAN_POINT('Origin',(0.,-2.,4.));
#10057=CARTESIAN_POINT('Origin',(0.,-1.7,4.));
#10058=CARTESIAN_POINT('',(-1.005,-1.5,4.));
#10059=CARTESIAN_POINT('Origin',(0.,-1.5,4.));
#10060=CARTESIAN_POINT('',(-1.005,-1.7,4.));
#10061=CARTESIAN_POINT('Origin',(0.,-1.7,4.));
#10062=CARTESIAN_POINT('',(-2.4,-1.5,4.));
#10063=CARTESIAN_POINT('Origin',(0.,-1.5,4.));
#10064=CARTESIAN_POINT('',(-2.4,-1.7,4.));
#10065=CARTESIAN_POINT('',(-2.4,-1.7,4.));
#10066=CARTESIAN_POINT('Origin',(0.,-1.7,4.));
#10067=CARTESIAN_POINT('Origin',(0.,-1.5,4.));
#10068=CARTESIAN_POINT('Origin',(0.,-1.7,4.));
#13197=UNCERTAINTY_MEASURE_WITH_UNIT(LENGTH_MEASURE(0.001),#13278,
'DISTANCE_ACCURACY_VALUE',
'Maximum model space distance between geometric entities at asserted c
onnectivities');
#13233=UNCERTAINTY_MEASURE_WITH_UNIT(LENGTH_MEASURE(0.001),#13278,
'DISTANCE_ACCURACY_VALUE',
'Maximum model space distance between geometric entities at asserted c
onnectivities');
#13241=(
GEOMETRIC_REPRESENTATION_CONTEXT(3)
GLOBAL_UNCERTAINTY_ASSIGNED_CONTEXT((#13197))
GLOBAL_UNIT_ASSIGNED_CONTEXT((#13278,#13280,#13281))
REPRESENTATION_CONTEXT('','3D')
);
#13277=(
GEOMETRIC_REPRESENTATION_CONTEXT(3)
GLOBAL_UNCERTAINTY_ASSIGNED_CONTEXT((#13233))
GLOBAL_UNIT_ASSIGNED_CONTEXT((#13278,#13280,#13281))
REPRESENTATION_CONTEXT('','3D')
);
#13278=(
LENGTH_UNIT()
NAMED_UNIT(*)
SI_UNIT(.CENTI.,.METRE.)
);
#13280=(
NAMED_UNIT(*)
PLANE_ANGLE_UNIT()
SI_UNIT($,.RADIAN.)
);
#13281=(
NAMED_UNIT(*)
SI_UNIT($,.STERADIAN.)
SOLID_ANGLE_UNIT()
);
#13289=SHAPE_DEFINITION_REPRESENTATION(#13332,#13446);
#13332=PRODUCT_DEFINITION_SHAPE('',$,#13490);
#13446=SHAPE_REPRESENTATION('',(#6956),#13241);
#13482=PRODUCT_DEFINITION_CONTEXT('part definition',#13613,'design');
#13490=PRODUCT_DEFINITION('Bearing cap (1)','Bearing cap (1)',#13533,#13482);
#13533=PRODUCT_DEFINITION_FORMATION('',$,#13622);
#13613=APPLICATION_CONTEXT(
'Core Data for Automotive Mechanical Design Process');
#13614=PRODUCT_CONTEXT('part definition',#13613,'mechanical');
#13622=PRODUCT('Bearing cap (1)','Bearing cap (1)','Bearing cap (1)',(#13614));
#13714=COLOUR_RGB('Grey',0.48,0.52,0.57);
#13715=FILL_AREA_STYLE_COLOUR('',#13714);
#13716=FILL_AREA_STYLE('',(#13715));
#13717=SURFACE_STYLE_FILL_AREA(#13716);
#13718=SURFACE_SIDE_STYLE('',(#13717));
#13719=SURFACE_STYLE_USAGE(.BOTH.,#13718);
#13720=PRESENTATION_STYLE_ASSIGNMENT((#13719));
ENDSEC;
END-ISO-10303-21;
